ISO-10303-21;
HEADER;
/* Generated by software containing ST-Developer
 * from STEP Tools, Inc. (www.steptools.com) 
 */

FILE_DESCRIPTION(
/* description */ (''),
/* implementation_level */ '2;1');

FILE_NAME(
/* name */ 'PO10.step',
/* time_stamp */ '2026-10-06T10:18:54-07:00',
/* author */ (''),
/* organization */ (''),
/* preprocessor_version */ 'ST-DEVELOPER v20.2',
/* originating_system */ 'Autodesk Translation Framework v15.15.0.0',
/* authorisation */ '');

FILE_SCHEMA (('AUTOMOTIVE_DESIGN { 1 0 10303 214 3 1 1 }'));
ENDSEC;

DATA;
#10=MECHANICAL_DESIGN_GEOMETRIC_PRESENTATION_REPRESENTATION('',(#84),#8445);
#66=SHAPE_REPRESENTATION_RELATIONSHIP('SRR','None',#8487,#75);
#75=ADVANCED_BREP_SHAPE_REPRESENTATION('',(#93),#8439);
#84=STYLED_ITEM('',(#8537),#93);
#93=MANIFOLD_SOLID_BREP('Body2',#4005);
#151=CYLINDRICAL_SURFACE('',#4371,3.);
#152=CYLINDRICAL_SURFACE('',#4387,5.);
#203=TOROIDAL_SURFACE('',#4366,4.,1.);
#204=TOROIDAL_SURFACE('',#4382,4.,1.);
#358=FACE_BOUND('',#951,.T.);
#359=FACE_BOUND('',#962,.T.);
#466=CIRCLE('',#4367,3.);
#467=CIRCLE('',#4368,1.);
#468=CIRCLE('',#4369,4.);
#469=CIRCLE('',#4370,3.);
#470=CIRCLE('',#4372,3.);
#471=CIRCLE('',#4374,5.);
#472=CIRCLE('',#4383,4.);
#473=CIRCLE('',#4384,1.);
#474=CIRCLE('',#4385,5.);
#475=CIRCLE('',#4386,5.);
#692=FACE_OUTER_BOUND('',#948,.T.);
#693=FACE_OUTER_BOUND('',#949,.T.);
#694=FACE_OUTER_BOUND('',#950,.T.);
#695=FACE_OUTER_BOUND('',#952,.T.);
#696=FACE_OUTER_BOUND('',#953,.T.);
#697=FACE_OUTER_BOUND('',#954,.T.);
#698=FACE_OUTER_BOUND('',#955,.T.);
#699=FACE_OUTER_BOUND('',#956,.T.);
#700=FACE_OUTER_BOUND('',#957,.T.);
#701=FACE_OUTER_BOUND('',#958,.T.);
#702=FACE_OUTER_BOUND('',#959,.T.);
#703=FACE_OUTER_BOUND('',#960,.T.);
#704=FACE_OUTER_BOUND('',#961,.T.);
#705=FACE_OUTER_BOUND('',#963,.T.);
#948=EDGE_LOOP('',(#3353,#3354,#3355,#3356,#3357));
#949=EDGE_LOOP('',(#3358,#3359,#3360,#3361,#3362));
#950=EDGE_LOOP('',(#3363));
#951=EDGE_LOOP('',(#3364));
#952=EDGE_LOOP('',(#3365,#3366,#3367,#3368));
#953=EDGE_LOOP('',(#3369,#3370,#3371,#3372));
#954=EDGE_LOOP('',(#3373,#3374,#3375,#3376));
#955=EDGE_LOOP('',(#3377,#3378,#3379,#3380));
#956=EDGE_LOOP('',(#3381,#3382,#3383,#3384));
#957=EDGE_LOOP('',(#3385,#3386,#3387,#3388));
#958=EDGE_LOOP('',(#3389,#3390,#3391,#3392,#3393,#3394));
#959=EDGE_LOOP('',(#3395,#3396,#3397,#3398,#3399));
#960=EDGE_LOOP('',(#3400,#3401,#3402,#3403,#3404));
#961=EDGE_LOOP('',(#3405));
#962=EDGE_LOOP('',(#3406,#3407,#3408,#3409,#3410,#3411));
#963=EDGE_LOOP('',(#3412));
#1227=LINE('',#8098,#1516);
#1228=LINE('',#8105,#1517);
#1229=LINE('',#8107,#1518);
#1230=LINE('',#8109,#1519);
#1231=LINE('',#8110,#1520);
#1232=LINE('',#8113,#1521);
#1233=LINE('',#8115,#1522);
#1234=LINE('',#8116,#1523);
#1235=LINE('',#8119,#1524);
#1236=LINE('',#8121,#1525);
#1237=LINE('',#8122,#1526);
#1238=LINE('',#8125,#1527);
#1239=LINE('',#8127,#1528);
#1240=LINE('',#8128,#1529);
#1241=LINE('',#8131,#1530);
#1242=LINE('',#8133,#1531);
#1243=LINE('',#8134,#1532);
#1244=LINE('',#8136,#1533);
#1245=LINE('',#8137,#1534);
#1246=LINE('',#8148,#1535);
#1516=VECTOR('',#5236,3.);
#1517=VECTOR('',#5243,10.);
#1518=VECTOR('',#5244,10.);
#1519=VECTOR('',#5245,10.);
#1520=VECTOR('',#5246,10.);
#1521=VECTOR('',#5249,10.);
#1522=VECTOR('',#5250,10.);
#1523=VECTOR('',#5251,10.);
#1524=VECTOR('',#5254,10.);
#1525=VECTOR('',#5255,10.);
#1526=VECTOR('',#5256,10.);
#1527=VECTOR('',#5259,10.);
#1528=VECTOR('',#5260,10.);
#1529=VECTOR('',#5261,10.);
#1530=VECTOR('',#5264,10.);
#1531=VECTOR('',#5265,10.);
#1532=VECTOR('',#5266,10.);
#1533=VECTOR('',#5269,10.);
#1534=VECTOR('',#5270,10.);
#1535=VECTOR('',#5285,5.);
#1864=VERTEX_POINT('',#8088);
#1865=VERTEX_POINT('',#8089);
#1866=VERTEX_POINT('',#8091);
#1867=VERTEX_POINT('',#8096);
#1868=VERTEX_POINT('',#8100);
#1869=VERTEX_POINT('',#8103);
#1870=VERTEX_POINT('',#8104);
#1871=VERTEX_POINT('',#8106);
#1872=VERTEX_POINT('',#8108);
#1873=VERTEX_POINT('',#8112);
#1874=VERTEX_POINT('',#8114);
#1875=VERTEX_POINT('',#8118);
#1876=VERTEX_POINT('',#8120);
#1877=VERTEX_POINT('',#8124);
#1878=VERTEX_POINT('',#8126);
#1879=VERTEX_POINT('',#8130);
#1880=VERTEX_POINT('',#8132);
#1881=VERTEX_POINT('',#8140);
#1882=VERTEX_POINT('',#8142);
#1883=VERTEX_POINT('',#8144);
#2377=EDGE_CURVE('',#1864,#1865,#466,.T.);
#2378=EDGE_CURVE('',#1865,#1866,#467,.T.);
#2379=EDGE_CURVE('',#1866,#1866,#468,.T.);
#2380=EDGE_CURVE('',#1865,#1864,#469,.T.);
#2381=EDGE_CURVE('',#1867,#1867,#470,.T.);
#2382=EDGE_CURVE('',#1867,#1864,#1227,.T.);
#2383=EDGE_CURVE('',#1868,#1868,#471,.T.);
#2384=EDGE_CURVE('',#1869,#1870,#1228,.T.);
#2385=EDGE_CURVE('',#1869,#1871,#1229,.T.);
#2386=EDGE_CURVE('',#1871,#1872,#1230,.T.);
#2387=EDGE_CURVE('',#1870,#1872,#1231,.T.);
#2388=EDGE_CURVE('',#1873,#1869,#1232,.T.);
#2389=EDGE_CURVE('',#1873,#1874,#1233,.T.);
#2390=EDGE_CURVE('',#1874,#1871,#1234,.T.);
#2391=EDGE_CURVE('',#1875,#1873,#1235,.T.);
#2392=EDGE_CURVE('',#1875,#1876,#1236,.T.);
#2393=EDGE_CURVE('',#1876,#1874,#1237,.T.);
#2394=EDGE_CURVE('',#1877,#1875,#1238,.T.);
#2395=EDGE_CURVE('',#1877,#1878,#1239,.T.);
#2396=EDGE_CURVE('',#1878,#1876,#1240,.T.);
#2397=EDGE_CURVE('',#1879,#1877,#1241,.T.);
#2398=EDGE_CURVE('',#1879,#1880,#1242,.T.);
#2399=EDGE_CURVE('',#1880,#1878,#1243,.T.);
#2400=EDGE_CURVE('',#1870,#1879,#1244,.T.);
#2401=EDGE_CURVE('',#1872,#1880,#1245,.T.);
#2402=EDGE_CURVE('',#1881,#1881,#472,.T.);
#2403=EDGE_CURVE('',#1881,#1882,#473,.T.);
#2404=EDGE_CURVE('',#1882,#1883,#474,.T.);
#2405=EDGE_CURVE('',#1883,#1882,#475,.T.);
#2406=EDGE_CURVE('',#1883,#1868,#1246,.T.);
#3353=ORIENTED_EDGE('',*,*,#2377,.T.);
#3354=ORIENTED_EDGE('',*,*,#2378,.T.);
#3355=ORIENTED_EDGE('',*,*,#2379,.T.);
#3356=ORIENTED_EDGE('',*,*,#2378,.F.);
#3357=ORIENTED_EDGE('',*,*,#2380,.T.);
#3358=ORIENTED_EDGE('',*,*,#2381,.F.);
#3359=ORIENTED_EDGE('',*,*,#2382,.T.);
#3360=ORIENTED_EDGE('',*,*,#2380,.F.);
#3361=ORIENTED_EDGE('',*,*,#2377,.F.);
#3362=ORIENTED_EDGE('',*,*,#2382,.F.);
#3363=ORIENTED_EDGE('',*,*,#2383,.T.);
#3364=ORIENTED_EDGE('',*,*,#2379,.F.);
#3365=ORIENTED_EDGE('',*,*,#2384,.F.);
#3366=ORIENTED_EDGE('',*,*,#2385,.T.);
#3367=ORIENTED_EDGE('',*,*,#2386,.T.);
#3368=ORIENTED_EDGE('',*,*,#2387,.F.);
#3369=ORIENTED_EDGE('',*,*,#2388,.F.);
#3370=ORIENTED_EDGE('',*,*,#2389,.T.);
#3371=ORIENTED_EDGE('',*,*,#2390,.T.);
#3372=ORIENTED_EDGE('',*,*,#2385,.F.);
#3373=ORIENTED_EDGE('',*,*,#2391,.F.);
#3374=ORIENTED_EDGE('',*,*,#2392,.T.);
#3375=ORIENTED_EDGE('',*,*,#2393,.T.);
#3376=ORIENTED_EDGE('',*,*,#2389,.F.);
#3377=ORIENTED_EDGE('',*,*,#2394,.F.);
#3378=ORIENTED_EDGE('',*,*,#2395,.T.);
#3379=ORIENTED_EDGE('',*,*,#2396,.T.);
#3380=ORIENTED_EDGE('',*,*,#2392,.F.);
#3381=ORIENTED_EDGE('',*,*,#2397,.F.);
#3382=ORIENTED_EDGE('',*,*,#2398,.T.);
#3383=ORIENTED_EDGE('',*,*,#2399,.T.);
#3384=ORIENTED_EDGE('',*,*,#2395,.F.);
#3385=ORIENTED_EDGE('',*,*,#2400,.F.);
#3386=ORIENTED_EDGE('',*,*,#2387,.T.);
#3387=ORIENTED_EDGE('',*,*,#2401,.T.);
#3388=ORIENTED_EDGE('',*,*,#2398,.F.);
#3389=ORIENTED_EDGE('',*,*,#2401,.F.);
#3390=ORIENTED_EDGE('',*,*,#2386,.F.);
#3391=ORIENTED_EDGE('',*,*,#2390,.F.);
#3392=ORIENTED_EDGE('',*,*,#2393,.F.);
#3393=ORIENTED_EDGE('',*,*,#2396,.F.);
#3394=ORIENTED_EDGE('',*,*,#2399,.F.);
#3395=ORIENTED_EDGE('',*,*,#2402,.T.);
#3396=ORIENTED_EDGE('',*,*,#2403,.T.);
#3397=ORIENTED_EDGE('',*,*,#2404,.T.);
#3398=ORIENTED_EDGE('',*,*,#2405,.T.);
#3399=ORIENTED_EDGE('',*,*,#2403,.F.);
#3400=ORIENTED_EDGE('',*,*,#2405,.F.);
#3401=ORIENTED_EDGE('',*,*,#2406,.T.);
#3402=ORIENTED_EDGE('',*,*,#2383,.F.);
#3403=ORIENTED_EDGE('',*,*,#2406,.F.);
#3404=ORIENTED_EDGE('',*,*,#2404,.F.);
#3405=ORIENTED_EDGE('',*,*,#2402,.F.);
#3406=ORIENTED_EDGE('',*,*,#2384,.T.);
#3407=ORIENTED_EDGE('',*,*,#2400,.T.);
#3408=ORIENTED_EDGE('',*,*,#2397,.T.);
#3409=ORIENTED_EDGE('',*,*,#2394,.T.);
#3410=ORIENTED_EDGE('',*,*,#2391,.T.);
#3411=ORIENTED_EDGE('',*,*,#2388,.T.);
#3412=ORIENTED_EDGE('',*,*,#2381,.T.);
#3720=PLANE('',#4373);
#3721=PLANE('',#4375);
#3722=PLANE('',#4376);
#3723=PLANE('',#4377);
#3724=PLANE('',#4378);
#3725=PLANE('',#4379);
#3726=PLANE('',#4380);
#3727=PLANE('',#4381);
#3728=PLANE('',#4388);
#3729=PLANE('',#4389);
#3933=ADVANCED_FACE('',(#692),#203,.F.);
#3934=ADVANCED_FACE('',(#693),#151,.T.);
#3935=ADVANCED_FACE('',(#694,#358),#3720,.T.);
#3936=ADVANCED_FACE('',(#695),#3721,.F.);
#3937=ADVANCED_FACE('',(#696),#3722,.F.);
#3938=ADVANCED_FACE('',(#697),#3723,.F.);
#3939=ADVANCED_FACE('',(#698),#3724,.F.);
#3940=ADVANCED_FACE('',(#699),#3725,.F.);
#3941=ADVANCED_FACE('',(#700),#3726,.F.);
#3942=ADVANCED_FACE('',(#701),#3727,.F.);
#3943=ADVANCED_FACE('',(#702),#204,.T.);
#3944=ADVANCED_FACE('',(#703),#152,.T.);
#3945=ADVANCED_FACE('',(#704,#359),#3728,.F.);
#3946=ADVANCED_FACE('',(#705),#3729,.T.);
#4005=CLOSED_SHELL('',(#3933,#3934,#3935,#3936,#3937,#3938,#3939,#3940,
#3941,#3942,#3943,#3944,#3945,#3946));
#4365=AXIS2_PLACEMENT_3D('',#8086,#5220,#5221);
#4366=AXIS2_PLACEMENT_3D('',#8087,#5222,#5223);
#4367=AXIS2_PLACEMENT_3D('',#8090,#5224,#5225);
#4368=AXIS2_PLACEMENT_3D('',#8092,#5226,#5227);
#4369=AXIS2_PLACEMENT_3D('',#8093,#5228,#5229);
#4370=AXIS2_PLACEMENT_3D('',#8094,#5230,#5231);
#4371=AXIS2_PLACEMENT_3D('',#8095,#5232,#5233);
#4372=AXIS2_PLACEMENT_3D('',#8097,#5234,#5235);
#4373=AXIS2_PLACEMENT_3D('',#8099,#5237,#5238);
#4374=AXIS2_PLACEMENT_3D('',#8101,#5239,#5240);
#4375=AXIS2_PLACEMENT_3D('',#8102,#5241,#5242);
#4376=AXIS2_PLACEMENT_3D('',#8111,#5247,#5248);
#4377=AXIS2_PLACEMENT_3D('',#8117,#5252,#5253);
#4378=AXIS2_PLACEMENT_3D('',#8123,#5257,#5258);
#4379=AXIS2_PLACEMENT_3D('',#8129,#5262,#5263);
#4380=AXIS2_PLACEMENT_3D('',#8135,#5267,#5268);
#4381=AXIS2_PLACEMENT_3D('',#8138,#5271,#5272);
#4382=AXIS2_PLACEMENT_3D('',#8139,#5273,#5274);
#4383=AXIS2_PLACEMENT_3D('',#8141,#5275,#5276);
#4384=AXIS2_PLACEMENT_3D('',#8143,#5277,#5278);
#4385=AXIS2_PLACEMENT_3D('',#8145,#5279,#5280);
#4386=AXIS2_PLACEMENT_3D('',#8146,#5281,#5282);
#4387=AXIS2_PLACEMENT_3D('',#8147,#5283,#5284);
#4388=AXIS2_PLACEMENT_3D('',#8149,#5286,#5287);
#4389=AXIS2_PLACEMENT_3D('',#8150,#5288,#5289);
#5220=DIRECTION('axis',(0.,0.,1.));
#5221=DIRECTION('refdir',(1.,0.,0.));
#5222=DIRECTION('center_axis',(-1.,0.,0.));
#5223=DIRECTION('ref_axis',(0.,0.,1.));
#5224=DIRECTION('center_axis',(-1.,0.,0.));
#5225=DIRECTION('ref_axis',(0.,1.,0.));
#5226=DIRECTION('center_axis',(0.,-1.,1.22464679914735E-16));
#5227=DIRECTION('ref_axis',(0.,-1.22464679914735E-16,-1.));
#5228=DIRECTION('center_axis',(1.,0.,0.));
#5229=DIRECTION('ref_axis',(0.,1.,0.));
#5230=DIRECTION('center_axis',(-1.,0.,0.));
#5231=DIRECTION('ref_axis',(0.,1.,0.));
#5232=DIRECTION('center_axis',(1.,0.,0.));
#5233=DIRECTION('ref_axis',(0.,1.,0.));
#5234=DIRECTION('center_axis',(1.,0.,0.));
#5235=DIRECTION('ref_axis',(0.,1.,0.));
#5236=DIRECTION('',(-1.,0.,0.));
#5237=DIRECTION('center_axis',(1.,0.,0.));
#5238=DIRECTION('ref_axis',(0.,1.,0.));
#5239=DIRECTION('center_axis',(1.,0.,0.));
#5240=DIRECTION('ref_axis',(0.,1.,0.));
#5241=DIRECTION('center_axis',(0.,-0.5,-0.866025403784439));
#5242=DIRECTION('ref_axis',(0.,0.866025403784439,-0.5));
#5243=DIRECTION('',(0.,0.866025403784439,-0.5));
#5244=DIRECTION('',(1.,0.,0.));
#5245=DIRECTION('',(0.,0.866025403784439,-0.5));
#5246=DIRECTION('',(1.,0.,0.));
#5247=DIRECTION('center_axis',(0.,-1.,-1.58603286868792E-16));
#5248=DIRECTION('ref_axis',(0.,1.58603286868792E-16,-1.));
#5249=DIRECTION('',(0.,1.58603286868792E-16,-1.));
#5250=DIRECTION('',(1.,0.,0.));
#5251=DIRECTION('',(0.,1.58603286868792E-16,-1.));
#5252=DIRECTION('center_axis',(0.,-0.5,0.866025403784439));
#5253=DIRECTION('ref_axis',(0.,-0.866025403784439,-0.5));
#5254=DIRECTION('',(0.,-0.866025403784439,-0.5));
#5255=DIRECTION('',(1.,0.,0.));
#5256=DIRECTION('',(0.,-0.866025403784439,-0.5));
#5257=DIRECTION('center_axis',(0.,0.5,0.866025403784439));
#5258=DIRECTION('ref_axis',(0.,-0.866025403784439,0.5));
#5259=DIRECTION('',(0.,-0.866025403784439,0.5));
#5260=DIRECTION('',(1.,0.,0.));
#5261=DIRECTION('',(0.,-0.866025403784439,0.5));
#5262=DIRECTION('center_axis',(0.,1.,3.17206573737584E-16));
#5263=DIRECTION('ref_axis',(0.,-3.17206573737584E-16,1.));
#5264=DIRECTION('',(0.,-3.17206573737584E-16,1.));
#5265=DIRECTION('',(1.,0.,0.));
#5266=DIRECTION('',(0.,-3.17206573737584E-16,1.));
#5267=DIRECTION('center_axis',(0.,0.5,-0.866025403784439));
#5268=DIRECTION('ref_axis',(0.,0.866025403784439,0.5));
#5269=DIRECTION('',(0.,0.866025403784439,0.5));
#5270=DIRECTION('',(0.,0.866025403784439,0.5));
#5271=DIRECTION('center_axis',(1.,0.,0.));
#5272=DIRECTION('ref_axis',(0.,0.,-1.));
#5273=DIRECTION('center_axis',(-1.,0.,0.));
#5274=DIRECTION('ref_axis',(0.,0.,1.));
#5275=DIRECTION('center_axis',(1.,0.,0.));
#5276=DIRECTION('ref_axis',(0.,1.,0.));
#5277=DIRECTION('center_axis',(0.,-1.,1.22464679914735E-16));
#5278=DIRECTION('ref_axis',(0.,-1.22464679914735E-16,-1.));
#5279=DIRECTION('center_axis',(-1.,0.,0.));
#5280=DIRECTION('ref_axis',(0.,1.,0.));
#5281=DIRECTION('center_axis',(-1.,0.,0.));
#5282=DIRECTION('ref_axis',(0.,1.,0.));
#5283=DIRECTION('center_axis',(-1.,0.,0.));
#5284=DIRECTION('ref_axis',(0.,1.,0.));
#5285=DIRECTION('',(1.,0.,0.));
#5286=DIRECTION('center_axis',(1.,0.,0.));
#5287=DIRECTION('ref_axis',(0.,1.,0.));
#5288=DIRECTION('center_axis',(1.,0.,0.));
#5289=DIRECTION('ref_axis',(0.,1.,0.));
#8086=CARTESIAN_POINT('',(0.,0.,0.));
#8087=CARTESIAN_POINT('Origin',(1.,0.,0.));
#8088=CARTESIAN_POINT('',(1.,-3.,3.67394039744206E-16));
#8089=CARTESIAN_POINT('',(1.,-3.67394039744206E-16,-3.));
#8090=CARTESIAN_POINT('Origin',(1.,0.,0.));
#8091=CARTESIAN_POINT('',(0.,-4.89858719658941E-16,-4.));
#8092=CARTESIAN_POINT('Origin',(1.,-4.89858719658941E-16,-4.));
#8093=CARTESIAN_POINT('Origin',(0.,0.,0.));
#8094=CARTESIAN_POINT('Origin',(1.,0.,0.));
#8095=CARTESIAN_POINT('Origin',(0.,0.,0.));
#8096=CARTESIAN_POINT('',(16.,-3.,-3.67394039744206E-16));
#8097=CARTESIAN_POINT('Origin',(16.,0.,0.));
#8098=CARTESIAN_POINT('',(0.,-3.,-3.67394039744206E-16));
#8099=CARTESIAN_POINT('Origin',(0.,0.,0.));
#8100=CARTESIAN_POINT('',(0.,-5.,-6.12323399573677E-16));
#8101=CARTESIAN_POINT('Origin',(0.,0.,0.));
#8102=CARTESIAN_POINT('Origin',(-3.5,-3.03108895841228,-1.75000002607703));
#8103=CARTESIAN_POINT('',(-3.5,-3.03108895841228,-1.75000002607703));
#8104=CARTESIAN_POINT('',(-3.5,0.,-3.50000005215406));
#8105=CARTESIAN_POINT('',(-3.5,-2.27331671880921,-2.18750003259629));
#8106=CARTESIAN_POINT('',(-1.5,-3.03108895841228,-1.75000002607703));
#8107=CARTESIAN_POINT('',(-3.5,-3.03108895841228,-1.75000002607703));
#8108=CARTESIAN_POINT('',(-1.5,0.,-3.50000005215406));
#8109=CARTESIAN_POINT('',(-1.5,0.,-3.50000005215406));
#8110=CARTESIAN_POINT('',(-3.5,0.,-3.50000005215406));
#8111=CARTESIAN_POINT('Origin',(-3.5,-3.03108895841228,1.75000002607703));
#8112=CARTESIAN_POINT('',(-3.5,-3.03108895841228,1.75000002607703));
#8113=CARTESIAN_POINT('',(-3.5,-3.03108895841228,0.875000013038516));
#8114=CARTESIAN_POINT('',(-1.5,-3.03108895841228,1.75000002607703));
#8115=CARTESIAN_POINT('',(-3.5,-3.03108895841228,1.75000002607703));
#8116=CARTESIAN_POINT('',(-1.5,-3.03108895841228,-1.75000002607703));
#8117=CARTESIAN_POINT('Origin',(-3.5,-1.11022302462516E-15,3.50000005215406));
#8118=CARTESIAN_POINT('',(-3.5,-8.32667268468867E-16,3.50000005215406));
#8119=CARTESIAN_POINT('',(-3.5,-0.757772239603071,3.06250004563481));
#8120=CARTESIAN_POINT('',(-1.5,-1.11022302462516E-15,3.50000005215406));
#8121=CARTESIAN_POINT('',(-3.5,-8.32667268468867E-16,3.50000005215406));
#8122=CARTESIAN_POINT('',(-1.5,-3.03108895841228,1.75000002607703));
#8123=CARTESIAN_POINT('Origin',(-3.5,3.03108895841228,1.75000002607703));
#8124=CARTESIAN_POINT('',(-3.5,3.03108895841228,1.75000002607703));
#8125=CARTESIAN_POINT('',(-3.5,2.27331671880921,2.18750003259629));
#8126=CARTESIAN_POINT('',(-1.5,3.03108895841228,1.75000002607703));
#8127=CARTESIAN_POINT('',(-3.5,3.03108895841228,1.75000002607703));
#8128=CARTESIAN_POINT('',(-1.5,-8.32667268468867E-16,3.50000005215406));
#8129=CARTESIAN_POINT('Origin',(-3.5,3.03108895841228,-1.75000002607703));
#8130=CARTESIAN_POINT('',(-3.5,3.03108895841228,-1.75000002607703));
#8131=CARTESIAN_POINT('',(-3.5,3.03108895841228,-0.875000013038515));
#8132=CARTESIAN_POINT('',(-1.5,3.03108895841228,-1.75000002607703));
#8133=CARTESIAN_POINT('',(-3.5,3.03108895841228,-1.75000002607703));
#8134=CARTESIAN_POINT('',(-1.5,3.03108895841228,1.75000002607703));
#8135=CARTESIAN_POINT('Origin',(-3.5,0.,-3.50000005215406));
#8136=CARTESIAN_POINT('',(-3.5,0.75777223960307,-3.06250004563481));
#8137=CARTESIAN_POINT('',(-1.5,3.03108895841228,-1.75000002607703));
#8138=CARTESIAN_POINT('Origin',(-1.5,0.,0.));
#8139=CARTESIAN_POINT('Origin',(-2.5,0.,0.));
#8140=CARTESIAN_POINT('',(-3.5,-4.89858719658941E-16,-4.));
#8141=CARTESIAN_POINT('Origin',(-3.5,0.,0.));
#8142=CARTESIAN_POINT('',(-2.5,-6.12323399573677E-16,-5.));
#8143=CARTESIAN_POINT('Origin',(-2.5,-4.89858719658941E-16,-4.));
#8144=CARTESIAN_POINT('',(-2.5,-5.,6.12323399573677E-16));
#8145=CARTESIAN_POINT('Origin',(-2.5,0.,0.));
#8146=CARTESIAN_POINT('Origin',(-2.5,0.,0.));
#8147=CARTESIAN_POINT('Origin',(0.,0.,0.));
#8148=CARTESIAN_POINT('',(0.,-5.,6.12323399573677E-16));
#8149=CARTESIAN_POINT('Origin',(-3.5,0.,0.));
#8150=CARTESIAN_POINT('Origin',(16.,0.,0.));
#8428=UNCERTAINTY_MEASURE_WITH_UNIT(LENGTH_MEASURE(0.01),#8446,
'DISTANCE_ACCURACY_VALUE',
'Maximum model space distance between geometric entities at asserted c
onnectivities');
#8434=UNCERTAINTY_MEASURE_WITH_UNIT(LENGTH_MEASURE(0.01),#8446,
'DISTANCE_ACCURACY_VALUE',
'Maximum model space distance between geometric entities at asserted c
onnectivities');
#8439=(
GEOMETRIC_REPRESENTATION_CONTEXT(3)
GLOBAL_UNCERTAINTY_ASSIGNED_CONTEXT((#8428))
GLOBAL_UNIT_ASSIGNED_CONTEXT((#8446,#8448,#8449))
REPRESENTATION_CONTEXT('','3D')
);
#8445=(
GEOMETRIC_REPRESENTATION_CONTEXT(3)
GLOBAL_UNCERTAINTY_ASSIGNED_CONTEXT((#8434))
GLOBAL_UNIT_ASSIGNED_CONTEXT((#8446,#8448,#8449))
REPRESENTATION_CONTEXT('','3D')
);
#8446=(
LENGTH_UNIT()
NAMED_UNIT(*)
SI_UNIT(.MILLI.,.METRE.)
);
#8448=(
NAMED_UNIT(*)
PLANE_ANGLE_UNIT()
SI_UNIT($,.RADIAN.)
);
#8449=(
NAMED_UNIT(*)
SI_UNIT($,.STERADIAN.)
SOLID_ANGLE_UNIT()
);
#8454=SHAPE_DEFINITION_REPRESENTATION(#8464,#8487);
#8464=PRODUCT_DEFINITION_SHAPE('',$,#8498);
#8487=SHAPE_REPRESENTATION('',(#4365),#8439);
#8493=PRODUCT_DEFINITION_CONTEXT('part definition',#8525,'design');
#8498=PRODUCT_DEFINITION('2026-10-05-11-50-53-123','PO10',#8508,#8493);
#8508=PRODUCT_DEFINITION_FORMATION('',$,#8531);
#8525=APPLICATION_CONTEXT(
'Core Data for Automotive Mechanical Design Process');
#8526=PRODUCT_CONTEXT('part definition',#8525,'mechanical');
#8531=PRODUCT('2026-10-05-11-50-53-123','PO10',$,(#8526));
#8537=PRESENTATION_STYLE_ASSIGNMENT((#8538));
#8538=SURFACE_STYLE_USAGE(.BOTH.,#8539);
#8539=SURFACE_SIDE_STYLE('',(#8540));
#8540=SURFACE_STYLE_FILL_AREA(#8541);
#8541=FILL_AREA_STYLE('Steel - Satin',(#8542));
#8542=FILL_AREA_STYLE_COLOUR('Steel - Satin',#8543);
#8543=COLOUR_RGB('Steel - Satin', 0.09019608, 0.27058824, 0.51372549);
ENDSEC;
END-ISO-10303-21;
